ISO-10303-21;
HEADER;
/* Generated by software containing ST-Developer
 * from STEP Tools, Inc. (www.steptools.com) 
 */

FILE_DESCRIPTION(
/* description */ (''),
/* implementation_level */ '2;1');

FILE_NAME(
/* name */ '12_ISO_2338_Tie_Pin_5x70.step',
/* time_stamp */ '2026-10-21T01:59:45-07:00',
/* author */ (''),
/* organization */ (''),
/* preprocessor_version */ 'ST-DEVELOPER v20.2',
/* originating_system */ 'Autodesk Translation Framework v15.15.0.0',
/* authorisation */ '');

FILE_SCHEMA (('AUTOMOTIVE_DESIGN { 1 0 10303 214 3 1 1 }'));
ENDSEC;

DATA;
#10=MECHANICAL_DESIGN_GEOMETRIC_PRESENTATION_REPRESENTATION('',(#480),#18281);
#435=CONICAL_SURFACE('',#9939,2.25,0.785398163397448);
#436=CONICAL_SURFACE('',#9943,2.25,0.78539816339745);
#449=SHAPE_REPRESENTATION_RELATIONSHIP('SRR','None',#18351,#462);
#462=ADVANCED_BREP_SHAPE_REPRESENTATION('',(#493),#18280);
#480=STYLED_ITEM('',(#18474),#493);
#493=MANIFOLD_SOLID_BREP('Body1',#9097);
#578=CYLINDRICAL_SURFACE('',#9941,2.5);
#818=CIRCLE('',#9938,2.);
#819=CIRCLE('',#9940,2.5);
#820=CIRCLE('',#9942,2.5);
#821=CIRCLE('',#9944,2.);
#1359=FACE_OUTER_BOUND('',#1931,.T.);
#1360=FACE_OUTER_BOUND('',#1932,.T.);
#1361=FACE_OUTER_BOUND('',#1933,.T.);
#1362=FACE_OUTER_BOUND('',#1934,.T.);
#1363=FACE_OUTER_BOUND('',#1935,.T.);
#1931=EDGE_LOOP('',(#8226));
#1932=EDGE_LOOP('',(#8227,#8228,#8229,#8230));
#1933=EDGE_LOOP('',(#8231,#8232,#8233,#8234));
#1934=EDGE_LOOP('',(#8235,#8236,#8237,#8238));
#1935=EDGE_LOOP('',(#8239));
#2778=LINE('',#18218,#3623);
#2779=LINE('',#18222,#3624);
#2780=LINE('',#18226,#3625);
#3623=VECTOR('',#12210,2.25);
#3624=VECTOR('',#12215,2.5);
#3625=VECTOR('',#12220,2.25);
#4414=VERTEX_POINT('',#18213);
#4415=VERTEX_POINT('',#18216);
#4416=VERTEX_POINT('',#18220);
#4417=VERTEX_POINT('',#18224);
#5685=EDGE_CURVE('',#4414,#4414,#818,.T.);
#5686=EDGE_CURVE('',#4415,#4415,#819,.T.);
#5687=EDGE_CURVE('',#4415,#4414,#2778,.T.);
#5688=EDGE_CURVE('',#4416,#4416,#820,.T.);
#5689=EDGE_CURVE('',#4416,#4415,#2779,.T.);
#5690=EDGE_CURVE('',#4417,#4417,#821,.T.);
#5691=EDGE_CURVE('',#4417,#4416,#2780,.T.);
#8226=ORIENTED_EDGE('',*,*,#5685,.F.);
#8227=ORIENTED_EDGE('',*,*,#5686,.F.);
#8228=ORIENTED_EDGE('',*,*,#5687,.T.);
#8229=ORIENTED_EDGE('',*,*,#5685,.T.);
#8230=ORIENTED_EDGE('',*,*,#5687,.F.);
#8231=ORIENTED_EDGE('',*,*,#5688,.F.);
#8232=ORIENTED_EDGE('',*,*,#5689,.T.);
#8233=ORIENTED_EDGE('',*,*,#5686,.T.);
#8234=ORIENTED_EDGE('',*,*,#5689,.F.);
#8235=ORIENTED_EDGE('',*,*,#5690,.F.);
#8236=ORIENTED_EDGE('',*,*,#5691,.T.);
#8237=ORIENTED_EDGE('',*,*,#5688,.T.);
#8238=ORIENTED_EDGE('',*,*,#5691,.F.);
#8239=ORIENTED_EDGE('',*,*,#5690,.T.);
#8561=PLANE('',#9937);
#8562=PLANE('',#9945);
#9080=ADVANCED_FACE('',(#1359),#8561,.T.);
#9081=ADVANCED_FACE('',(#1360),#435,.T.);
#9082=ADVANCED_FACE('',(#1361),#578,.T.);
#9083=ADVANCED_FACE('',(#1362),#436,.T.);
#9084=ADVANCED_FACE('',(#1363),#8562,.T.);
#9097=CLOSED_SHELL('',(#9080,#9081,#9082,#9083,#9084));
#9936=AXIS2_PLACEMENT_3D('',#18211,#12200,#12201);
#9937=AXIS2_PLACEMENT_3D('',#18212,#12202,#12203);
#9938=AXIS2_PLACEMENT_3D('',#18214,#12204,#12205);
#9939=AXIS2_PLACEMENT_3D('',#18215,#12206,#12207);
#9940=AXIS2_PLACEMENT_3D('',#18217,#12208,#12209);
#9941=AXIS2_PLACEMENT_3D('',#18219,#12211,#12212);
#9942=AXIS2_PLACEMENT_3D('',#18221,#12213,#12214);
#9943=AXIS2_PLACEMENT_3D('',#18223,#12216,#12217);
#9944=AXIS2_PLACEMENT_3D('',#18225,#12218,#12219);
#9945=AXIS2_PLACEMENT_3D('',#18227,#12221,#12222);
#12200=DIRECTION('axis',(0.,0.,1.));
#12201=DIRECTION('refdir',(1.,0.,0.));
#12202=DIRECTION('center_axis',(-1.,0.,0.));
#12203=DIRECTION('ref_axis',(0.,0.,1.));
#12204=DIRECTION('center_axis',(1.,0.,0.));
#12205=DIRECTION('ref_axis',(0.,0.,-1.));
#12206=DIRECTION('center_axis',(1.,0.,0.));
#12207=DIRECTION('ref_axis',(0.,1.,0.));
#12208=DIRECTION('center_axis',(1.,0.,0.));
#12209=DIRECTION('ref_axis',(0.,0.,-1.));
#12210=DIRECTION('',(-0.707106781186548,0.707106781186547,8.65956056235493E-17));
#12211=DIRECTION('center_axis',(1.,0.,0.));
#12212=DIRECTION('ref_axis',(0.,1.,0.));
#12213=DIRECTION('center_axis',(1.,0.,0.));
#12214=DIRECTION('ref_axis',(0.,0.,-1.));
#12215=DIRECTION('',(-1.,0.,0.));
#12216=DIRECTION('center_axis',(-1.,0.,0.));
#12217=DIRECTION('ref_axis',(0.,1.,0.));
#12218=DIRECTION('center_axis',(1.,0.,0.));
#12219=DIRECTION('ref_axis',(0.,0.,-1.));
#12220=DIRECTION('',(-0.707106781186546,-0.707106781186549,-8.65956056235495E-17));
#12221=DIRECTION('center_axis',(1.,0.,0.));
#12222=DIRECTION('ref_axis',(0.,0.,-1.));
#18211=CARTESIAN_POINT('',(0.,0.,0.));
#18212=CARTESIAN_POINT('Origin',(0.,2.,0.));
#18213=CARTESIAN_POINT('',(1.73472347597681E-15,-2.,-2.4492935982947E-16));
#18214=CARTESIAN_POINT('Origin',(0.,0.,0.));
#18215=CARTESIAN_POINT('Origin',(0.250000000000004,0.,0.));
#18216=CARTESIAN_POINT('',(0.500000000000001,-2.5,-3.06161699786838E-16));
#18217=CARTESIAN_POINT('Origin',(0.499999999999998,0.,0.));
#18218=CARTESIAN_POINT('',(0.250000000000004,-2.25,-2.75545529808154E-16));
#18219=CARTESIAN_POINT('Origin',(35.,0.,0.));
#18220=CARTESIAN_POINT('',(69.5,-2.5,-3.06161699786838E-16));
#18221=CARTESIAN_POINT('Origin',(69.5,0.,0.));
#18222=CARTESIAN_POINT('',(35.,-2.5,-3.06161699786838E-16));
#18223=CARTESIAN_POINT('Origin',(69.75,0.,0.));
#18224=CARTESIAN_POINT('',(70.,-2.,-2.4492935982947E-16));
#18225=CARTESIAN_POINT('Origin',(70.,0.,0.));
#18226=CARTESIAN_POINT('',(69.75,-2.25,-2.75545529808154E-16));
#18227=CARTESIAN_POINT('Origin',(70.,0.,0.));
#18265=UNCERTAINTY_MEASURE_WITH_UNIT(LENGTH_MEASURE(0.01),#18282,
'DISTANCE_ACCURACY_VALUE',
'Maximum model space distance between geometric entities at asserted c
onnectivities');
#18266=UNCERTAINTY_MEASURE_WITH_UNIT(LENGTH_MEASURE(0.01),#18282,
'DISTANCE_ACCURACY_VALUE',
'Maximum model space distance between geometric entities at asserted c
onnectivities');
#18280=(
GEOMETRIC_REPRESENTATION_CONTEXT(3)
GLOBAL_UNCERTAINTY_ASSIGNED_CONTEXT((#18265))
GLOBAL_UNIT_ASSIGNED_CONTEXT((#18282,#18284,#18285))
REPRESENTATION_CONTEXT('','3D')
);
#18281=(
GEOMETRIC_REPRESENTATION_CONTEXT(3)
GLOBAL_UNCERTAINTY_ASSIGNED_CONTEXT((#18266))
GLOBAL_UNIT_ASSIGNED_CONTEXT((#18282,#18284,#18285))
REPRESENTATION_CONTEXT('','3D')
);
#18282=(
LENGTH_UNIT()
NAMED_UNIT(*)
SI_UNIT(.MILLI.,.METRE.)
);
#18284=(
NAMED_UNIT(*)
PLANE_ANGLE_UNIT()
SI_UNIT($,.RADIAN.)
);
#18285=(
NAMED_UNIT(*)
SI_UNIT($,.STERADIAN.)
SOLID_ANGLE_UNIT()
);
#18299=SHAPE_DEFINITION_REPRESENTATION(#18313,#18351);
#18313=PRODUCT_DEFINITION_SHAPE('',$,#18366);
#18351=SHAPE_REPRESENTATION('',(#9936),#18280);
#18352=PRODUCT_DEFINITION_CONTEXT('part definition',#18396,'design');
#18366=PRODUCT_DEFINITION('2026-10-20-13-03-26-880',
'12_ISO_2338_Tie_Pin_5x70',#18380,#18352);
#18380=PRODUCT_DEFINITION_FORMATION('',$,#18411);
#18396=APPLICATION_CONTEXT(
'Core Data for Automotive Mechanical Design Process');
#18397=PRODUCT_CONTEXT('part definition',#18396,'mechanical');
#18411=PRODUCT('2026-10-20-13-03-26-880','12_ISO_2338_Tie_Pin_5x70',$,(#18397));
#18468=COLOUR_RGB('Grey',0.48,0.52,0.57);
#18469=FILL_AREA_STYLE_COLOUR('',#18468);
#18470=FILL_AREA_STYLE('',(#18469));
#18471=SURFACE_STYLE_FILL_AREA(#18470);
#18472=SURFACE_SIDE_STYLE('',(#18471));
#18473=SURFACE_STYLE_USAGE(.BOTH.,#18472);
#18474=PRESENTATION_STYLE_ASSIGNMENT((#18473));
ENDSEC;
END-ISO-10303-21;
